ISO-10303-21;
HEADER;
/* Generated by software containing ST-Developer
 * from STEP Tools, Inc. (www.steptools.com) 
 */

FILE_DESCRIPTION(
/* description */ ('PAT-082'),
/* implementation_level */ '2;1');

FILE_NAME(
/* name */ 'Cover locating dowel (1).step',
/* time_stamp */ '2026-10-29T20:16:13-07:00',
/* author */ (''),
/* organization */ (''),
/* preprocessor_version */ 'ST-DEVELOPER v20.2',
/* originating_system */ 'Autodesk Translation Framework v15.17.0.0',
/* authorisation */ '');

FILE_SCHEMA (('AUTOMOTIVE_DESIGN { 1 0 10303 214 3 1 1 }'));
ENDSEC;

DATA;
#10=MECHANICAL_DESIGN_GEOMETRIC_PRESENTATION_REPRESENTATION('',(#255),#8266);
#211=SHAPE_REPRESENTATION_RELATIONSHIP('SRR','None',#8373,#233);
#233=ADVANCED_BREP_SHAPE_REPRESENTATION('',(#277),#8257);
#255=STYLED_ITEM('',(#8530),#277);
#277=MANIFOLD_SOLID_BREP('Body1',#4595);
#506=PLANE('',#5188);
#507=PLANE('',#5189);
#744=FACE_OUTER_BOUND('',#1117,.T.);
#745=FACE_OUTER_BOUND('',#1118,.T.);
#746=FACE_OUTER_BOUND('',#1119,.T.);
#1117=EDGE_LOOP('',(#3848,#3849,#3850,#3851));
#1118=EDGE_LOOP('',(#3852));
#1119=EDGE_LOOP('',(#3853));
#1456=LINE('',#7770,#1811);
#1811=VECTOR('',#6279,0.15);
#2093=CIRCLE('',#5186,0.15);
#2094=CIRCLE('',#5187,0.15);
#2399=VERTEX_POINT('',#7767);
#2400=VERTEX_POINT('',#7769);
#2900=EDGE_CURVE('',#2399,#2399,#2093,.T.);
#2901=EDGE_CURVE('',#2399,#2400,#1456,.T.);
#2902=EDGE_CURVE('',#2400,#2400,#2094,.T.);
#3848=ORIENTED_EDGE('',*,*,#2900,.F.);
#3849=ORIENTED_EDGE('',*,*,#2901,.T.);
#3850=ORIENTED_EDGE('',*,*,#2902,.T.);
#3851=ORIENTED_EDGE('',*,*,#2901,.F.);
#3852=ORIENTED_EDGE('',*,*,#2900,.T.);
#3853=ORIENTED_EDGE('',*,*,#2902,.F.);
#4291=CYLINDRICAL_SURFACE('',#5185,0.15);
#4483=ADVANCED_FACE('',(#744),#4291,.T.);
#4484=ADVANCED_FACE('',(#745),#506,.T.);
#4485=ADVANCED_FACE('',(#746),#507,.F.);
#4595=CLOSED_SHELL('',(#4483,#4484,#4485));
#5184=AXIS2_PLACEMENT_3D('',#7765,#6273,#6274);
#5185=AXIS2_PLACEMENT_3D('',#7766,#6275,#6276);
#5186=AXIS2_PLACEMENT_3D('',#7768,#6277,#6278);
#5187=AXIS2_PLACEMENT_3D('',#7771,#6280,#6281);
#5188=AXIS2_PLACEMENT_3D('',#7772,#6282,#6283);
#5189=AXIS2_PLACEMENT_3D('',#7773,#6284,#6285);
#6273=DIRECTION('axis',(0.,0.,1.));
#6274=DIRECTION('refdir',(1.,0.,0.));
#6275=DIRECTION('center_axis',(0.,0.,1.));
#6276=DIRECTION('ref_axis',(1.,0.,0.));
#6277=DIRECTION('center_axis',(0.,0.,1.));
#6278=DIRECTION('ref_axis',(1.,0.,0.));
#6279=DIRECTION('',(0.,0.,-1.));
#6280=DIRECTION('center_axis',(0.,0.,1.));
#6281=DIRECTION('ref_axis',(1.,0.,0.));
#6282=DIRECTION('center_axis',(0.,0.,1.));
#6283=DIRECTION('ref_axis',(1.,0.,0.));
#6284=DIRECTION('center_axis',(0.,0.,1.));
#6285=DIRECTION('ref_axis',(1.,0.,0.));
#7765=CARTESIAN_POINT('',(0.,0.,0.));
#7766=CARTESIAN_POINT('Origin',(5.,0.,1.6));
#7767=CARTESIAN_POINT('',(4.85,-1.83697019872103E-17,2.3));
#7768=CARTESIAN_POINT('Origin',(5.,0.,2.3));
#7769=CARTESIAN_POINT('',(4.85,-1.83697019872103E-17,1.6));
#7770=CARTESIAN_POINT('',(4.85,-1.83697019872103E-17,1.6));
#7771=CARTESIAN_POINT('Origin',(5.,0.,1.6));
#7772=CARTESIAN_POINT('Origin',(5.,0.,2.3));
#7773=CARTESIAN_POINT('Origin',(5.,0.,1.6));
#8232=UNCERTAINTY_MEASURE_WITH_UNIT(LENGTH_MEASURE(0.001),#8267,
'DISTANCE_ACCURACY_VALUE',
'Maximum model space distance between geometric entities at asserted c
onnectivities');
#8241=UNCERTAINTY_MEASURE_WITH_UNIT(LENGTH_MEASURE(0.001),#8267,
'DISTANCE_ACCURACY_VALUE',
'Maximum model space distance between geometric entities at asserted c
onnectivities');
#8257=(
GEOMETRIC_REPRESENTATION_CONTEXT(3)
GLOBAL_UNCERTAINTY_ASSIGNED_CONTEXT((#8232))
GLOBAL_UNIT_ASSIGNED_CONTEXT((#8267,#8269,#8270))
REPRESENTATION_CONTEXT('','3D')
);
#8266=(
GEOMETRIC_REPRESENTATION_CONTEXT(3)
GLOBAL_UNCERTAINTY_ASSIGNED_CONTEXT((#8241))
GLOBAL_UNIT_ASSIGNED_CONTEXT((#8267,#8269,#8270))
REPRESENTATION_CONTEXT('','3D')
);
#8267=(
LENGTH_UNIT()
NAMED_UNIT(*)
SI_UNIT(.CENTI.,.METRE.)
);
#8269=(
NAMED_UNIT(*)
PLANE_ANGLE_UNIT()
SI_UNIT($,.RADIAN.)
);
#8270=(
NAMED_UNIT(*)
SI_UNIT($,.STERADIAN.)
SOLID_ANGLE_UNIT()
);
#8286=SHAPE_DEFINITION_REPRESENTATION(#8310,#8373);
#8310=PRODUCT_DEFINITION_SHAPE('',$,#8398);
#8373=SHAPE_REPRESENTATION('',(#5184),#8257);
#8382=PRODUCT_DEFINITION_CONTEXT('part definition',#8456,'design');
#8398=PRODUCT_DEFINITION('Cover locating dowel (1)',
'Cover locating dowel (1)',#8422,#8382);
#8422=PRODUCT_DEFINITION_FORMATION('',$,#8473);
#8456=APPLICATION_CONTEXT(
'Core Data for Automotive Mechanical Design Process');
#8457=PRODUCT_CONTEXT('part definition',#8456,'mechanical');
#8473=PRODUCT('Cover locating dowel (1)','Cover locating dowel (1)',
'Cover locating dowel (1)',(#8457));
#8524=COLOUR_RGB('Sky Blue',0.24,0.69,0.87);
#8525=FILL_AREA_STYLE_COLOUR('',#8524);
#8526=FILL_AREA_STYLE('',(#8525));
#8527=SURFACE_STYLE_FILL_AREA(#8526);
#8528=SURFACE_SIDE_STYLE('',(#8527));
#8529=SURFACE_STYLE_USAGE(.BOTH.,#8528);
#8530=PRESENTATION_STYLE_ASSIGNMENT((#8529));
ENDSEC;
END-ISO-10303-21;
